ISO-10303-21;
HEADER;
FILE_DESCRIPTION (('STEP AP214'),
    '1' );
FILE_NAME ('socket head cap screw_iso_ISO 4762 M4 x 6 - 6N.step',
    '2026-10-24T04:45:50',
    ( '' ),
    ( '' ),
    'SwSTEP 2.0',
    'SolidWorks 2026',
    '' );
FILE_SCHEMA (( 'AUTOMOTIVE_DESIGN' ));
ENDSEC;

DATA;
#5=ADVANCED_FACE ( 'NONE', ( #1217, #1180 ), #2474, .T. ) ;
#8=DIRECTION ( 'NONE',  ( 0.000000000000000000, 0.000000000000000000, -1.000000000000000000 ) ) ;
#14=FACE_OUTER_BOUND ( 'NONE', #3102, .T. ) ;
#21=VERTEX_POINT ( 'NONE', #149 ) ;
#27=CARTESIAN_POINT ( 'NONE',  ( 2.000000000000000000, -1.773042676681341856, 2.276824562219559311E-15 ) ) ;
#28=VERTEX_POINT ( 'NONE', #3019 ) ;
#31=DIRECTION ( 'NONE',  ( -0.7071067811865355823, 0.000000000000000000, 0.7071067811865595631 ) ) ;
#33=LINE ( 'NONE', #1363, #814 ) ;
#34=ORIENTED_EDGE ( 'NONE', *, *, #997, .F. ) ;
#36=EDGE_CURVE ( 'NONE', #859, #595, #2266, .T. ) ;
#42=AXIS2_PLACEMENT_3D ( 'NONE', #131, #167, #900 ) ;
#45=LINE ( 'NONE', #1904, #2060 ) ;
#56=ORIENTED_EDGE ( 'NONE', *, *, #736, .T. ) ;
#57=ORIENTED_EDGE ( 'NONE', *, *, #3226, .F. ) ;
#61=ORIENTED_EDGE ( 'NONE', *, *, #3226, .T. ) ;
#64=EDGE_LOOP ( 'NONE', ( #1744, #977, #3089, #1709 ) ) ;
#71=ORIENTED_EDGE ( 'NONE', *, *, #288, .F. ) ;
#73=DIRECTION ( 'NONE',  ( 0.000000000000000000, -0.8660254037844391517, -0.4999999999999991673 ) ) ;
#75=FACE_OUTER_BOUND ( 'NONE', #670, .T. ) ;
#79=LINE ( 'NONE', #829, #260 ) ;
#85=EDGE_LOOP ( 'NONE', ( #3218, #1338, #850, #555, #3293 ) ) ;
#86=CARTESIAN_POINT ( 'NONE',  ( 4.000000000000000000, 0.000000000000000000, 0.000000000000000000 ) ) ;
#89=LINE ( 'NONE', #1159, #2710 ) ;
#90=EDGE_CURVE ( 'NONE', #872, #1203, #2433, .T. ) ;
#95=CARTESIAN_POINT ( 'NONE',  ( 0.1999999999999987899, 4.286263797015736595E-16, -3.500000000000000000 ) ) ;
#100=ORIENTED_EDGE ( 'NONE', *, *, #3033, .T. ) ;
#104=AXIS2_PLACEMENT_3D ( 'NONE', #3003, #1688, #391 ) ;
#110=DIRECTION ( 'NONE',  ( -1.000000000000000000, -0.000000000000000000, -0.000000000000000000 ) ) ;
#117=CARTESIAN_POINT ( 'NONE',  ( 9.610000000000013642, 2.449293598294707893E-16, -2.000000000000000888 ) ) ;
#131=CARTESIAN_POINT ( 'NONE',  ( 10.00000000000000000, 1.610000000000000098, 0.000000000000000000 ) ) ;
#135=FACE_OUTER_BOUND ( 'NONE', #3028, .T. ) ;
#138=ORIENTED_EDGE ( 'NONE', *, *, #2911, .T. ) ;
#139=CARTESIAN_POINT ( 'NONE',  ( 10.00000000000000178, 0.000000000000000000, 0.000000000000000000 ) ) ;
#144=EDGE_CURVE ( 'NONE', #1979, #3353, #770, .T. ) ;
#147=CIRCLE ( 'NONE', #1023, 2.000000000000000888 ) ;
#149=CARTESIAN_POINT ( 'NONE',  ( 4.000000000000001776, 0.000000000000000000, -2.200000000000001066 ) ) ;
#151=DIRECTION ( 'NONE',  ( 1.000000000000000000, 0.000000000000000000, 0.000000000000000000 ) ) ;
#154=VECTOR ( 'NONE', #3115, 1000.000000000000114 ) ;
#155=ORIENTED_EDGE ( 'NONE', *, *, #2097, .T. ) ;
#157=VECTOR ( 'NONE', #2892, 1000.000000000000227 ) ;
#159=EDGE_CURVE ( 'NONE', #28, #1965, #1834, .T. ) ;
#163=DIRECTION ( 'NONE',  ( -1.000000000000000000, -0.000000000000000000, -0.000000000000000000 ) ) ;
#166=FACE_OUTER_BOUND ( 'NONE', #3168, .T. ) ;
#167=DIRECTION ( 'NONE',  ( 1.000000000000000000, 0.000000000000000000, 0.000000000000000000 ) ) ;
#171=PLANE ( 'NONE',  #1465 ) ;
#182=DIRECTION ( 'NONE',  ( 0.000000000000000000, 0.4999999999999989453, -0.8660254037844391517 ) ) ;
#184=LINE ( 'NONE', #1230, #2344 ) ;
#187=ADVANCED_FACE ( 'NONE', ( #2861 ), #2830, .F. ) ;
#199=DIRECTION ( 'NONE',  ( 0.000000000000000000, 0.000000000000000000, -1.000000000000000000 ) ) ;
#200=EDGE_LOOP ( 'NONE', ( #2592, #100, #1336, #1799 ) ) ;
#204=LINE ( 'NONE', #550, #154 ) ;
#205=EDGE_CURVE ( 'NONE', #575, #3353, #2981, .T. ) ;
#210=CIRCLE ( 'NONE', #2393, 0.2000000000000000944 ) ;
#212=AXIS2_PLACEMENT_3D ( 'NONE', #1617, #2642, #885 ) ;
#220=EDGE_CURVE ( 'NONE', #2968, #788, #147, .T. ) ;
#221=DIRECTION ( 'NONE',  ( 0.000000000000000000, 0.4999999999999989453, -0.8660254037844391517 ) ) ;
#223=VERTEX_POINT ( 'NONE', #2047 ) ;
#225=FACE_OUTER_BOUND ( 'NONE', #834, .T. ) ;
#230=( NAMED_UNIT ( * ) SI_UNIT ( $, .STERADIAN. ) SOLID_ANGLE_UNIT ( ) );
#231=CARTESIAN_POINT ( 'NONE',  ( 2.000000000000000000, 1.773042676681340524, -2.059984127722458425E-15 ) ) ;
#244=DIRECTION ( 'NONE',  ( 0.000000000000000000, 0.000000000000000000, 1.000000000000000000 ) ) ;
#249=CARTESIAN_POINT ( 'NONE',  ( 0.000000000000000000, 0.8865213383406715941, 1.535499999999999199 ) ) ;
#257=CIRCLE ( 'NONE', #2169, 0.2000000000000000944 ) ;
#258=EDGE_LOOP ( 'NONE', ( #2050, #2619 ) ) ;
#260=VECTOR ( 'NONE', #1128, 1000.000000000000000 ) ;
#262=CIRCLE ( 'NONE', #1350, 1.610000000000000098 ) ;
#269=VECTOR ( 'NONE', #221, 1000.000000000000227 ) ;
#272=DIRECTION ( 'NONE',  ( 1.000000000000000000, 0.000000000000000000, 0.000000000000000000 ) ) ;
#273=PRODUCT_DEFINITION ( 'UNKNOWN', '', #2401, #2052 ) ;
#274=CARTESIAN_POINT ( 'NONE',  ( 2.000000000000000000, -1.773042676681341856, 2.276824562219559311E-15 ) ) ;
#281=ORIENTED_EDGE ( 'NONE', *, *, #304, .T. ) ;
#284=( NAMED_UNIT ( * ) SI_UNIT ( $, .STERADIAN. ) SOLID_ANGLE_UNIT ( ) );
#288=EDGE_CURVE ( 'NONE', #788, #2968, #3262, .T. ) ;
#293=ORIENTED_EDGE ( 'NONE', *, *, #658, .F. ) ;
#295=EDGE_CURVE ( 'NONE', #1203, #575, #3205, .T. ) ;
#297=ORIENTED_EDGE ( 'NONE', *, *, #467, .F. ) ;
#303=PLANE ( 'NONE',  #477 ) ;
#304=EDGE_CURVE ( 'NONE', #820, #28, #1614, .T. ) ;
#306=ORIENTED_EDGE ( 'NONE', *, *, #1644, .T. ) ;
#319=DIRECTION ( 'NONE',  ( 0.000000000000000000, -1.000000000000000000, 0.000000000000000000 ) ) ;
#321=LINE ( 'NONE', #1331, #636 ) ;
#334=SHAPE_REPRESENTATION_RELATIONSHIP ( 'NONE' , 'NONE' ,  #1286, #3149 ) ;
#335=ORIENTED_EDGE ( 'NONE', *, *, #1134, .T. ) ;
#337=FACE_OUTER_BOUND ( 'NONE', #2632, .T. ) ;
#338=CARTESIAN_POINT ( 'NONE',  ( 2.000000000000000000, 0.8865213383406680414, -1.535500000000000975 ) ) ;
#343=EDGE_CURVE ( 'NONE', #2100, #2365, #797, .T. ) ;
#346=DIRECTION ( 'NONE',  ( -1.000000000000000000, -0.000000000000000000, -0.000000000000000000 ) ) ;
#352=EDGE_CURVE ( 'NONE', #2026, #820, #262, .T. ) ;
#354=ORIENTED_EDGE ( 'NONE', *, *, #2172, .F. ) ;
#363=LINE ( 'NONE', #1728, #583 ) ;
#366=AXIS2_PLACEMENT_3D ( 'NONE', #1458, #3294, #1985 ) ;
#367=FACE_OUTER_BOUND ( 'NONE', #3150, .T. ) ;
#371=DIRECTION ( 'NONE',  ( -1.000000000000000000, -0.000000000000000000, -0.000000000000000000 ) ) ;
#374=EDGE_CURVE ( 'NONE', #2968, #21, #257, .T. ) ;
#378=CIRCLE ( 'NONE', #212, 3.500000000000000000 ) ;
#383=CARTESIAN_POINT ( 'NONE',  ( 2.000000000000000000, 0.000000000000000000, 0.000000000000000000 ) ) ;
#387=AXIS2_PLACEMENT_3D ( 'NONE', #2488, #151, #2249 ) ;
#389=ADVANCED_FACE ( 'NONE', ( #337 ), #751, .T. ) ;
#391=DIRECTION ( 'NONE',  ( 0.000000000000000000, 1.224646799147353207E-16, 1.000000000000000000 ) ) ;
#395=CARTESIAN_POINT ( 'NONE',  ( 2.000000000000000000, -0.8865213383406694847, 1.535500000000001419 ) ) ;
#396=APPLICATION_CONTEXT ( 'automotive_design' ) ;
#397=DIRECTION ( 'NONE',  ( 0.000000000000000000, 0.4999999999999991118, -0.8660254037844390407 ) ) ;
#401=PRODUCT_CONTEXT ( 'NONE', #1167, 'mechanical' ) ;
#416=EDGE_CURVE ( 'NONE', #2252, #436, #1895, .T. ) ;
#428=AXIS2_PLACEMENT_3D ( 'NONE', #139, #1256, #3320 ) ;
#431=AXIS2_PLACEMENT_3D ( 'NONE', #2899, #2590, #546 ) ;
#436=VERTEX_POINT ( 'NONE', #95 ) ;
#438=STYLED_ITEM ( 'NONE', ( #1597 ), #3149 ) ;
#440=ORIENTED_EDGE ( 'NONE', *, *, #90, .F. ) ;
#446=DIRECTION ( 'NONE',  ( -0.000000000000000000, 0.8660254037844392627, 0.4999999999999990008 ) ) ;
#462=ORIENTED_EDGE ( 'NONE', *, *, #144, .F. ) ;
#467=EDGE_CURVE ( 'NONE', #2054, #940, #3232, .T. ) ;
#474=AXIS2_PLACEMENT_3D ( 'NONE', #3365, #715, #2588 ) ;
#477=AXIS2_PLACEMENT_3D ( 'NONE', #2403, #3181, #1342 ) ;
#488=VECTOR ( 'NONE', #2883, 1000.000000000000000 ) ;
#502=ORIENTED_EDGE ( 'NONE', *, *, #2853, .F. ) ;
#512=ORIENTED_EDGE ( 'NONE', *, *, #2624, .F. ) ;
#514=PLANE ( 'NONE',  #2007 ) ;
#519=ORIENTED_EDGE ( 'NONE', *, *, #1564, .F. ) ;
#522=DIRECTION ( 'NONE',  ( 0.000000000000000000, -0.5000000000000011102, -0.8660254037844379305 ) ) ;
#527=DIRECTION ( 'NONE',  ( -1.000000000000000000, -0.000000000000000000, -0.000000000000000000 ) ) ;
#528=ADVANCED_FACE ( 'NONE', ( #914 ), #2517, .T. ) ;
#533=CARTESIAN_POINT ( 'NONE',  ( 0.000000000000000000, 0.8865213383406680414, -1.535500000000000975 ) ) ;
#543=CARTESIAN_POINT ( 'NONE',  ( 2.000000000000000000, 0.8865213383406680414, -1.535500000000000975 ) ) ;
#544=DIRECTION ( 'NONE',  ( -1.000000000000000000, -0.000000000000000000, -0.000000000000000000 ) ) ;
#545=EDGE_CURVE ( 'NONE', #28, #788, #2244, .T. ) ;
#546=DIRECTION ( 'NONE',  ( 0.000000000000000000, 0.000000000000000000, 1.000000000000000000 ) ) ;
#550=CARTESIAN_POINT ( 'NONE',  ( 10.00000000000000178, 1.971681346627238735E-16, -1.610000000000000098 ) ) ;
#555=ORIENTED_EDGE ( 'NONE', *, *, #2172, .T. ) ;
#556=ADVANCED_FACE ( 'NONE', ( #3015, #1192 ), #2228, .T. ) ;
#563=DIRECTION ( 'NONE',  ( -1.000000000000000000, -0.000000000000000000, -0.000000000000000000 ) ) ;
#566=CARTESIAN_POINT ( 'NONE',  ( 0.000000000000000000, 1.773042676681340524, -2.059984127722458425E-15 ) ) ;
#567=( LENGTH_UNIT ( ) NAMED_UNIT ( * ) SI_UNIT ( .MILLI., .METRE. ) );
#570=ADVANCED_FACE ( 'NONE', ( #166 ), #1717, .T. ) ;
#571=DIRECTION ( 'NONE',  ( 1.000000000000000000, 0.000000000000000000, 0.000000000000000000 ) ) ;
#572=FACE_OUTER_BOUND ( 'NONE', #3302, .T. ) ;
#573=MANIFOLD_SOLID_BREP ( 'Hex', #3148 ) ;
#575=VERTEX_POINT ( 'NONE', #1278 ) ;
#576=ORIENTED_EDGE ( 'NONE', *, *, #343, .T. ) ;
#582=ORIENTED_EDGE ( 'NONE', *, *, #2378, .T. ) ;
#583=VECTOR ( 'NONE', #2735, 1000.000000000000114 ) ;
#587=DIRECTION ( 'NONE',  ( 0.000000000000000000, 0.000000000000000000, 1.000000000000000000 ) ) ;
#588=ADVANCED_FACE ( 'NONE', ( #367 ), #2004, .F. ) ;
#591=AXIS2_PLACEMENT_3D ( 'NONE', #86, #1136, #2168 ) ;
#592=DIRECTION ( 'NONE',  ( -1.000000000000000000, -0.000000000000000000, -0.000000000000000000 ) ) ;
#595=VERTEX_POINT ( 'NONE', #1562 ) ;
#599=ORIENTED_EDGE ( 'NONE', *, *, #2055, .T. ) ;
#601=FILL_AREA_STYLE_COLOUR ( '', #3001 ) ;
#604=CARTESIAN_POINT ( 'NONE',  ( 2.000000000000000000, 0.8865213383406680414, -1.535500000000000975 ) ) ;
#605=CARTESIAN_POINT ( 'NONE',  ( 2.000000000000000000, 0.000000000000000000, 0.000000000000000000 ) ) ;
#607=CARTESIAN_POINT ( 'NONE',  ( 2.000000000000000000, -1.773042676681341856, 2.276824562219559311E-15 ) ) ;
#621=DIRECTION ( 'NONE',  ( 0.000000000000000000, 0.000000000000000000, 1.000000000000000000 ) ) ;
#622=DIRECTION ( 'NONE',  ( -1.000000000000000000, -0.000000000000000000, -0.000000000000000000 ) ) ;
#629=LINE ( 'NONE', #2695, #2935 ) ;
#636=VECTOR ( 'NONE', #2965, 1000.000000000000000 ) ;
#640=CIRCLE ( 'NONE', #1461, 1.610000000000000098 ) ;
#644=TOROIDAL_SURFACE ( 'NONE', #1847, 3.299999999999999822, 0.2000000000000000111 ) ;
#648=AXIS2_PLACEMENT_3D ( 'NONE', #1364, #592, #1637 ) ;
#658=EDGE_CURVE ( 'NONE', #223, #872, #1457, .T. ) ;
#668=DIRECTION ( 'NONE',  ( 0.000000000000000000, -0.5000000000000011102, -0.8660254037844379305 ) ) ;
#670=EDGE_LOOP ( 'NONE', ( #138, #56, #2676, #1810 ) ) ;
#683=CARTESIAN_POINT ( 'NONE',  ( 2.000000000000000000, -1.502314598737159426E-15, -1.535500000000000087 ) ) ;
#694=LINE ( 'NONE', #1446, #867 ) ;
#697=TOROIDAL_SURFACE ( 'NONE', #1628, 2.200000000000001066, 0.2000000000000000111 ) ;
#708=EDGE_CURVE ( 'NONE', #3353, #2365, #1789, .T. ) ;
#712=CARTESIAN_POINT ( 'NONE',  ( 0.000000000000000000, 0.000000000000000000, 0.000000000000000000 ) ) ;
#715=DIRECTION ( 'NONE',  ( -1.000000000000000000, -0.000000000000000000, -0.000000000000000000 ) ) ;
#723=ORIENTED_EDGE ( 'NONE', *, *, #2943, .F. ) ;
#730=DIRECTION ( 'NONE',  ( 0.000000000000000000, 0.000000000000000000, 1.000000000000000000 ) ) ;
#736=EDGE_CURVE ( 'NONE', #1395, #436, #629, .T. ) ;
#745=DIRECTION ( 'NONE',  ( -1.000000000000000000, -0.000000000000000000, -0.000000000000000000 ) ) ;
#751=CONICAL_SURFACE ( 'NONE', #2655, 1.610000000000000098, 0.7853981633974652654 ) ;
#754=VECTOR ( 'NONE', #1951, 1000.000000000000000 ) ;
#755=CONICAL_SURFACE ( 'NONE', #2177, 1.535500000000000087, 1.047197551196590748 ) ;
#770=LINE ( 'NONE', #1806, #2815 ) ;
#773=CARTESIAN_POINT ( 'NONE',  ( 0.1999999999999987899, 0.000000000000000000, 0.000000000000000000 ) ) ;
#775=ORIENTED_EDGE ( 'NONE', *, *, #886, .F. ) ;
#776=DIRECTION ( 'NONE',  ( 1.000000000000000000, 0.000000000000000000, 0.000000000000000000 ) ) ;
#779=PLANE ( 'NONE',  #1736 ) ;
#788=VERTEX_POINT ( 'NONE', #2445 ) ;
#794=EDGE_CURVE ( 'NONE', #1979, #575, #89, .T. ) ;
#797=LINE ( 'NONE', #543, #3212 ) ;
#802=LINE ( 'NONE', #2887, #863 ) ;
#804=ADVANCED_FACE ( 'NONE', ( #14 ), #755, .F. ) ;
#807=VECTOR ( 'NONE', #3083, 1000.000000000000000 ) ;
#808=DIRECTION ( 'NONE',  ( 0.000000000000000000, 1.000000000000000000, -9.783878858594328898E-16 ) ) ;
#814=VECTOR ( 'NONE', #1147, 1000.000000000000000 ) ;
#819=LINE ( 'NONE', #3143, #488 ) ;
#820=VERTEX_POINT ( 'NONE', #3202 ) ;
#829=CARTESIAN_POINT ( 'NONE',  ( 2.000000000000000000, 1.773042676681340524, -2.059984127722458425E-15 ) ) ;
#834=EDGE_LOOP ( 'NONE', ( #1103, #3022, #2540, #2748 ) ) ;
#841=LINE ( 'NONE', #533, #1409 ) ;
#844=ORIENTED_EDGE ( 'NONE', *, *, #736, .F. ) ;
#846=ADVANCED_FACE ( 'NONE', ( #75 ), #1125, .T. ) ;
#850=ORIENTED_EDGE ( 'NONE', *, *, #794, .T. ) ;
#859=VERTEX_POINT ( 'NONE', #2036 ) ;
#863=VECTOR ( 'NONE', #1523, 1000.000000000000114 ) ;
#867=VECTOR ( 'NONE', #1248, 1000.000000000000000 ) ;
#870=AXIS2_PLACEMENT_3D ( 'NONE', #3071, #2860, #2062 ) ;
#872=VERTEX_POINT ( 'NONE', #1235 ) ;
#873=DIRECTION ( 'NONE',  ( 0.000000000000000000, -1.224646799147353207E-16, 1.000000000000000000 ) ) ;
#878=DIRECTION ( 'NONE',  ( 0.000000000000000000, 0.000000000000000000, 1.000000000000000000 ) ) ;
#880=VERTEX_POINT ( 'NONE', #2292 ) ;
#885=DIRECTION ( 'NONE',  ( 0.000000000000000000, 0.000000000000000000, 1.000000000000000000 ) ) ;
#886=EDGE_CURVE ( 'NONE', #2365, #2834, #2218, .T. ) ;
#887=VERTEX_POINT ( 'NONE', #1746 ) ;
#889=CARTESIAN_POINT ( 'NONE',  ( 0.1999999999999987899, 4.041334437186265510E-16, -3.299999999999999822 ) ) ;
#890=CARTESIAN_POINT ( 'NONE',  ( 2.000000000000000000, -0.8865213383406694847, 1.535500000000001419 ) ) ;
#892=EDGE_LOOP ( 'NONE', ( #1598, #2085, #61, #1335, #2189 ) ) ;
#898=EDGE_CURVE ( 'NONE', #872, #1926, #2783, .T. ) ;
#899=CARTESIAN_POINT ( 'NONE',  ( 0.000000000000000000, -1.773042676681341856, 2.276824562219559311E-15 ) ) ;
#900=DIRECTION ( 'NONE',  ( 0.000000000000000000, 0.000000000000000000, -1.000000000000000000 ) ) ;
#903=DIRECTION ( 'NONE',  ( 0.000000000000000000, -0.4999999999999989453, 0.8660254037844391517 ) ) ;
#904=FACE_OUTER_BOUND ( 'NONE', #85, .T. ) ;
#905=EDGE_LOOP ( 'NONE', ( #1623, #1912, #1670 ) ) ;
#908=ORIENTED_EDGE ( 'NONE', *, *, #2303, .F. ) ;
#914=FACE_OUTER_BOUND ( 'NONE', #200, .T. ) ;
#918=ADVANCED_FACE ( 'NONE', ( #2479 ), #1899, .T. ) ;
#919=VECTOR ( 'NONE', #2073, 1000.000000000000000 ) ;
#923=CARTESIAN_POINT ( 'NONE',  ( 0.000000000000000000, 0.000000000000000000, 0.000000000000000000 ) ) ;
#932=SHAPE_DEFINITION_REPRESENTATION ( #2611, #1286 ) ;
#940=VERTEX_POINT ( 'NONE', #1436 ) ;
#947=ORIENTED_EDGE ( 'NONE', *, *, #1080, .T. ) ;
#963=PLANE ( 'NONE',  #1092 ) ;
#964=EDGE_LOOP ( 'NONE', ( #1584, #2798, #775, #3184, #2217 ) ) ;
#976=AXIS2_PLACEMENT_3D ( 'NONE', #2536, #446, #903 ) ;
#977=ORIENTED_EDGE ( 'NONE', *, *, #416, .F. ) ;
#979=CIRCLE ( 'NONE', #2716, 0.2000000000000000944 ) ;
#997=EDGE_CURVE ( 'NONE', #2026, #1965, #204, .T. ) ;
#1003=CARTESIAN_POINT ( 'NONE',  ( 0.000000000000000000, -1.773042676681341856, 2.276824562219559311E-15 ) ) ;
#1011=FACE_OUTER_BOUND ( 'NONE', #1227, .T. ) ;
#1019=DIRECTION ( 'NONE',  ( 0.000000000000000000, 0.000000000000000000, 1.000000000000000000 ) ) ;
#1023=AXIS2_PLACEMENT_3D ( 'NONE', #2606, #272, #1316 ) ;
#1032=AXIS2_PLACEMENT_3D ( 'NONE', #1228, #2298, #1782 ) ;
#1035=ORIENTED_EDGE ( 'NONE', *, *, #1068, .T. ) ;
#1040=ADVANCED_FACE ( 'NONE', ( #1011 ), #1517, .T. ) ;
#1042=DIRECTION ( 'NONE',  ( 0.000000000000000000, 0.000000000000000000, -1.000000000000000000 ) ) ;
#1049=EDGE_LOOP ( 'NONE', ( #2630, #1234 ) ) ;
#1051=LINE ( 'NONE', #2087, #2501 ) ;
#1054=VERTEX_POINT ( 'NONE', #1322 ) ;
#1059=LINE ( 'NONE', #231, #2064 ) ;
#1061=DIRECTION ( 'NONE',  ( 1.000000000000000000, 0.000000000000000000, 0.000000000000000000 ) ) ;
#1065=ORIENTED_EDGE ( 'NONE', *, *, #3024, .T. ) ;
#1067=ORIENTED_EDGE ( 'NONE', *, *, #2876, .F. ) ;
#1068=EDGE_CURVE ( 'NONE', #3353, #2100, #802, .T. ) ;
#1071=SURFACE_STYLE_FILL_AREA ( #2669 ) ;
#1075=DIRECTION ( 'NONE',  ( -1.000000000000000000, -0.000000000000000000, -0.000000000000000000 ) ) ;
#1077=CARTESIAN_POINT ( 'NONE',  ( 4.200000000000001954, 0.000000000000000000, -2.200000000000001066 ) ) ;
#1080=EDGE_CURVE ( 'NONE', #2072, #1203, #1299, .T. ) ;
#1081=ORIENTED_EDGE ( 'NONE', *, *, #2552, .T. ) ;
#1082=ORIENTED_EDGE ( 'NONE', *, *, #2552, .F. ) ;
#1087=ORIENTED_EDGE ( 'NONE', *, *, #304, .F. ) ;
#1091=( NAMED_UNIT ( * ) SI_UNIT ( $, .STERADIAN. ) SOLID_ANGLE_UNIT ( ) );
#1092=AXIS2_PLACEMENT_3D ( 'NONE', #1999, #3328, #808 ) ;
#1094=ORIENTED_EDGE ( 'NONE', *, *, #1564, .T. ) ;
#1099=CARTESIAN_POINT ( 'NONE',  ( 10.00000000000000178, 0.000000000000000000, 0.000000000000000000 ) ) ;
#1101=( GEOMETRIC_REPRESENTATION_CONTEXT ( 3 ) GLOBAL_UNCERTAINTY_ASSIGNED_CONTEXT ( ( #2836 ) ) GLOBAL_UNIT_ASSIGNED_CONTEXT ( ( #1780, #1627, #284 ) ) REPRESENTATION_CONTEXT ( 'NONE', 'WORKASPACE' ) );
#1103=ORIENTED_EDGE ( 'NONE', *, *, #1913, .F. ) ;
#1107=ADVANCED_FACE ( 'NONE', ( #225 ), #3217, .F. ) ;
#1116=DIRECTION ( 'NONE',  ( -1.000000000000000000, -0.000000000000000000, -0.000000000000000000 ) ) ;
#1125=CYLINDRICAL_SURFACE ( 'NONE', #1572, 3.500000000000000000 ) ;
#1127=ADVANCED_FACE ( 'NONE', ( #2854 ), #514, .F. ) ;
#1128=DIRECTION ( 'NONE',  ( 0.000000000000000000, -0.4999999999999991118, 0.8660254037844391517 ) ) ;
#1134=EDGE_CURVE ( 'NONE', #2834, #940, #1051, .T. ) ;
#1136=DIRECTION ( 'NONE',  ( -1.000000000000000000, -0.000000000000000000, -0.000000000000000000 ) ) ;
#1143=CARTESIAN_POINT ( 'NONE',  ( 2.000000000000000000, 0.000000000000000000, 0.000000000000000000 ) ) ;
#1146=CARTESIAN_POINT ( 'NONE',  ( 4.200000000000001954, 0.000000000000000000, 0.000000000000000000 ) ) ;
#1147=DIRECTION ( 'NONE',  ( -1.000000000000000000, -0.000000000000000000, -0.000000000000000000 ) ) ;
#1158=ORIENTED_EDGE ( 'NONE', *, *, #374, .F. ) ;
#1159=CARTESIAN_POINT ( 'NONE',  ( 2.000000000000000000, 1.773042676681340524, -2.059984127722458425E-15 ) ) ;
#1167=APPLICATION_CONTEXT ( 'automotive_design' ) ;
#1176=ORIENTED_EDGE ( 'NONE', *, *, #2378, .F. ) ;
#1180=FACE_OUTER_BOUND ( 'NONE', #3074, .T. ) ;
#1192=FACE_OUTER_BOUND ( 'NONE', #1049, .T. ) ;
#1203=VERTEX_POINT ( 'NONE', #2190 ) ;
#1206=EDGE_CURVE ( 'NONE', #436, #859, #210, .T. ) ;
#1212=CARTESIAN_POINT ( 'NONE',  ( 0.1999999999999987899, 0.000000000000000000, 3.500000000000000000 ) ) ;
#1217=FACE_BOUND ( 'NONE', #2427, .T. ) ;
#1219=DIRECTION ( 'NONE',  ( -0.000000000000000000, 1.345283343056720273E-15, 1.000000000000000000 ) ) ;
#1227=EDGE_LOOP ( 'NONE', ( #723, #1351, #1260, #502 ) ) ;
#1228=CARTESIAN_POINT ( 'NONE',  ( 2.000000000000000000, 0.000000000000000000, 0.000000000000000000 ) ) ;
#1230=CARTESIAN_POINT ( 'NONE',  ( 2.000000000000000000, -0.8865213383406694847, 1.535500000000001419 ) ) ;
#1231=DIRECTION ( 'NONE',  ( 0.000000000000000000, 0.000000000000000000, 1.000000000000000000 ) ) ;
#1234=ORIENTED_EDGE ( 'NONE', *, *, #3013, .F. ) ;
#1235=CARTESIAN_POINT ( 'NONE',  ( 2.000000000000000000, -1.329782007511005837, 0.7677500000000023750 ) ) ;
#1236=AXIS2_PLACEMENT_3D ( 'NONE', #2505, #3032, #1989 ) ;
#1238=DIRECTION ( 'NONE',  ( 0.000000000000000000, 0.5000000000000011102, 0.8660254037844379305 ) ) ;
#1245=( GEOMETRIC_REPRESENTATION_CONTEXT ( 3 ) GLOBAL_UNCERTAINTY_ASSIGNED_CONTEXT ( ( #2091 ) ) GLOBAL_UNIT_ASSIGNED_CONTEXT ( ( #3069, #2845, #230 ) ) REPRESENTATION_CONTEXT ( 'NONE', 'WORKASPACE' ) );
#1248=DIRECTION ( 'NONE',  ( -1.000000000000000000, -0.000000000000000000, -0.000000000000000000 ) ) ;
#1256=DIRECTION ( 'NONE',  ( -1.000000000000000000, -0.000000000000000000, -0.000000000000000000 ) ) ;
#1260=ORIENTED_EDGE ( 'NONE', *, *, #1908, .F. ) ;
#1274=VERTEX_POINT ( 'NONE', #2422 ) ;
#1276=EDGE_CURVE ( 'NONE', #21, #887, #2069, .T. ) ;
#1278=CARTESIAN_POINT ( 'NONE',  ( 2.000000000000000000, 1.329782007511006281, 0.7677499999999984892 ) ) ;
#1281=CARTESIAN_POINT ( 'NONE',  ( 2.000000000000000000, 1.773042676681340524, -2.059984127722458425E-15 ) ) ;
#1286=SHAPE_REPRESENTATION ( 'socket head cap screw_iso_ISO 4762 M4 x 6 - 6N', ( #3111 ), #1101 ) ;
#1294=AXIS2_PLACEMENT_3D ( 'NONE', #1281, #1061, #1770 ) ;
#1299=LINE ( 'NONE', #2564, #919 ) ;
#1303=ORIENTED_EDGE ( 'NONE', *, *, #2303, .T. ) ;
#1305=CIRCLE ( 'NONE', #431, 3.500000000000000000 ) ;
#1307=DIRECTION ( 'NONE',  ( 0.000000000000000000, 0.8660254037844380415, -0.5000000000000012212 ) ) ;
#1316=DIRECTION ( 'NONE',  ( 0.000000000000000000, 0.000000000000000000, -1.000000000000000000 ) ) ;
#1322=CARTESIAN_POINT ( 'NONE',  ( 2.000000000000000000, -0.8865213383406694847, 1.535500000000001419 ) ) ;
#1331=CARTESIAN_POINT ( 'NONE',  ( 0.000000000000000000, 1.773042676681340524, -2.059984127722458425E-15 ) ) ;
#1335=ORIENTED_EDGE ( 'NONE', *, *, #898, .T. ) ;
#1336=ORIENTED_EDGE ( 'NONE', *, *, #220, .T. ) ;
#1338=ORIENTED_EDGE ( 'NONE', *, *, #2015, .F. ) ;
#1342=DIRECTION ( 'NONE',  ( 0.000000000000000000, 0.000000000000000000, -1.000000000000000000 ) ) ;
#1346=ADVANCED_FACE ( 'NONE', ( #2985 ), #1990, .T. ) ;
#1350=AXIS2_PLACEMENT_3D ( 'NONE', #1099, #3160, #587 ) ;
#1351=ORIENTED_EDGE ( 'NONE', *, *, #1206, .T. ) ;
#1358=ADVANCED_FACE ( 'NONE', ( #135 ), #171, .F. ) ;
#1363=CARTESIAN_POINT ( 'NONE',  ( -31.74999999999995737, 0.000000000000000000, 3.500000000000000000 ) ) ;
#1364=CARTESIAN_POINT ( 'NONE',  ( 9.610000000000013642, 0.000000000000000000, 0.000000000000000000 ) ) ;
#1366=ORIENTED_EDGE ( 'NONE', *, *, #3013, .T. ) ;
#1369=EDGE_CURVE ( 'NONE', #1054, #2078, #694, .T. ) ;
#1385=ORIENTED_EDGE ( 'NONE', *, *, #545, .T. ) ;
#1388=( NAMED_UNIT ( * ) PLANE_ANGLE_UNIT ( ) SI_UNIT ( $, .RADIAN. ) );
#1392=DIRECTION ( 'NONE',  ( 0.000000000000000000, 0.000000000000000000, 1.000000000000000000 ) ) ;
#1395=VERTEX_POINT ( 'NONE', #1757 ) ;
#1396=EDGE_LOOP ( 'NONE', ( #1863, #2412, #1553, #462, #3275 ) ) ;
#1399=CARTESIAN_POINT ( 'NONE',  ( -31.74999999999995737, 0.000000000000000000, 0.000000000000000000 ) ) ;
#1401=EDGE_LOOP ( 'NONE', ( #1831, #519, #3370 ) ) ;
#1409=VECTOR ( 'NONE', #1582, 1000.000000000000000 ) ;
#1413=DIRECTION ( 'NONE',  ( -1.000000000000000000, -0.000000000000000000, -0.000000000000000000 ) ) ;
#1415=CARTESIAN_POINT ( 'NONE',  ( -31.74999999999995737, 2.449293598294707893E-16, -2.000000000000000888 ) ) ;
#1422=ADVANCED_FACE ( 'NONE', ( #1497 ), #1708, .F. ) ;
#1423=ORIENTED_EDGE ( 'NONE', *, *, #295, .F. ) ;
#1428=LINE ( 'NONE', #3027, #754 ) ;
#1436=CARTESIAN_POINT ( 'NONE',  ( 0.000000000000000000, -0.8865213383406730374, -1.535499999999999421 ) ) ;
#1441=DIRECTION ( 'NONE',  ( -1.000000000000000000, -0.000000000000000000, -0.000000000000000000 ) ) ;
#1446=CARTESIAN_POINT ( 'NONE',  ( 2.000000000000000000, -0.8865213383406694847, 1.535500000000001419 ) ) ;
#1457=CIRCLE ( 'NONE', #1032, 1.535500000000000087 ) ;
#1458=CARTESIAN_POINT ( 'NONE',  ( -31.74999999999995737, 0.000000000000000000, 0.000000000000000000 ) ) ;
#1461=AXIS2_PLACEMENT_3D ( 'NONE', #2499, #163, #244 ) ;
#1465=AXIS2_PLACEMENT_3D ( 'NONE', #395, #1219, #2795 ) ;
#1466=DIRECTION ( 'NONE',  ( -1.000000000000000000, -0.000000000000000000, -0.000000000000000000 ) ) ;
#1473=ADVANCED_FACE ( 'NONE', ( #3128 ), #644, .T. ) ;
#1477=DIRECTION ( 'NONE',  ( 0.000000000000000000, 1.000000000000000000, -1.345283343056720273E-15 ) ) ;
#1491=ORIENTED_EDGE ( 'NONE', *, *, #3017, .F. ) ;
#1497=FACE_OUTER_BOUND ( 'NONE', #1401, .T. ) ;
#1498=EDGE_LOOP ( 'NONE', ( #71, #2016, #2376, #1158 ) ) ;
#1512=AXIS2_PLACEMENT_3D ( 'NONE', #605, #1116, #1886 ) ;
#1516=CARTESIAN_POINT ( 'NONE',  ( 0.1999999999999987899, 0.000000000000000000, 0.000000000000000000 ) ) ;
#1517=TOROIDAL_SURFACE ( 'NONE', #3158, 3.299999999999999822, 0.2000000000000000111 ) ;
#1523=DIRECTION ( 'NONE',  ( 0.000000000000000000, -0.5000000000000011102, -0.8660254037844379305 ) ) ;
#1537=CARTESIAN_POINT ( 'NONE',  ( 2.000000000000000000, -0.8865213383406730374, -1.535499999999999421 ) ) ;
#1546=DIRECTION ( 'NONE',  ( 1.000000000000000000, 0.000000000000000000, 0.000000000000000000 ) ) ;
#1548=PLANE ( 'NONE',  #870 ) ;
#1553=ORIENTED_EDGE ( 'NONE', *, *, #1068, .F. ) ;
#1562=CARTESIAN_POINT ( 'NONE',  ( 0.000000000000000000, 0.000000000000000000, 3.299999999999999822 ) ) ;
#1564=EDGE_CURVE ( 'NONE', #223, #2834, #2880, .T. ) ;
#1568=VECTOR ( 'NONE', #182, 1000.000000000000227 ) ;
#1572=AXIS2_PLACEMENT_3D ( 'NONE', #2156, #3225, #878 ) ;
#1582=DIRECTION ( 'NONE',  ( 0.000000000000000000, -1.000000000000000000, 9.783878858594328898E-16 ) ) ;
#1584=ORIENTED_EDGE ( 'NONE', *, *, #2521, .T. ) ;
#1593=CARTESIAN_POINT ( 'NONE',  ( 0.1999999999999987899, 0.000000000000000000, 0.000000000000000000 ) ) ;
#1597=PRESENTATION_STYLE_ASSIGNMENT (( #1647 ) ) ;
#1598=ORIENTED_EDGE ( 'NONE', *, *, #2097, .F. ) ;
#1608=ORIENTED_EDGE ( 'NONE', *, *, #352, .F. ) ;
#1614=LINE ( 'NONE', #2162, #1729 ) ;
#1617=CARTESIAN_POINT ( 'NONE',  ( 4.000000000000003553, 0.000000000000000000, 0.000000000000000000 ) ) ;
#1622=VECTOR ( 'NONE', #622, 1000.000000000000000 ) ;
#1623=ORIENTED_EDGE ( 'NONE', *, *, #794, .F. ) ;
#1627=( NAMED_UNIT ( * ) PLANE_ANGLE_UNIT ( ) SI_UNIT ( $, .RADIAN. ) );
#1628=AXIS2_PLACEMENT_3D ( 'NONE', #3239, #2693, #1695 ) ;
#1631=CARTESIAN_POINT ( 'NONE',  ( 2.886521338340684917, 0.000000000000000000, 0.000000000000000000 ) ) ;
#1637=DIRECTION ( 'NONE',  ( 0.000000000000000000, 0.000000000000000000, 1.000000000000000000 ) ) ;
#1638=ADVANCED_FACE ( 'NONE', ( #572 ), #303, .F. ) ;
#1644=EDGE_CURVE ( 'NONE', #2597, #3240, #321, .T. ) ;
#1647=SURFACE_STYLE_USAGE ( .BOTH. , #2426 ) ;
#1655=ORIENTED_EDGE ( 'NONE', *, *, #1661, .T. ) ;
#1661=EDGE_CURVE ( 'NONE', #1274, #2252, #33, .T. ) ;
#1664=CARTESIAN_POINT ( 'NONE',  ( 2.000000000000000000, 1.773042676681340524, -2.059984127722458425E-15 ) ) ;
#1665=CARTESIAN_POINT ( 'NONE',  ( -31.74999999999995737, 0.000000000000000000, 2.000000000000000888 ) ) ;
#1670=ORIENTED_EDGE ( 'NONE', *, *, #205, .F. ) ;
#1671=EDGE_LOOP ( 'NONE', ( #1082, #2782, #293 ) ) ;
#1672=DIRECTION ( 'NONE',  ( -0.000000000000000000, 1.000000000000000000, 1.224646799147353207E-16 ) ) ;
#1673=LINE ( 'NONE', #890, #1952 ) ;
#1675=DIRECTION ( 'NONE',  ( -1.000000000000000000, -0.000000000000000000, -0.000000000000000000 ) ) ;
#1688=DIRECTION ( 'NONE',  ( 0.000000000000000000, 1.000000000000000000, -1.224646799147353207E-16 ) ) ;
#1689=CIRCLE ( 'NONE', #2010, 3.299999999999999822 ) ;
#1695=DIRECTION ( 'NONE',  ( 0.000000000000000000, 0.000000000000000000, -1.000000000000000000 ) ) ;
#1708=PLANE ( 'NONE',  #387 ) ;
#1709=ORIENTED_EDGE ( 'NONE', *, *, #36, .F. ) ;
#1717=CYLINDRICAL_SURFACE ( 'NONE', #366, 3.500000000000000000 ) ;
#1728=CARTESIAN_POINT ( 'NONE',  ( 0.000000000000000000, 1.773042676681340524, -2.059984127722458425E-15 ) ) ;
#1729=VECTOR ( 'NONE', #31, 1000.000000000000114 ) ;
#1733=ORIENTED_EDGE ( 'NONE', *, *, #352, .T. ) ;
#1734=DIRECTION ( 'NONE',  ( 1.000000000000000000, 0.000000000000000000, 0.000000000000000000 ) ) ;
#1735=PLANE ( 'NONE',  #42 ) ;
#1736=AXIS2_PLACEMENT_3D ( 'NONE', #1816, #1307, #1238 ) ;
#1742=EDGE_CURVE ( 'NONE', #2100, #880, #2674, .T. ) ;
#1744=ORIENTED_EDGE ( 'NONE', *, *, #1206, .F. ) ;
#1746=CARTESIAN_POINT ( 'NONE',  ( 4.000000000000001776, 2.694222958124178486E-16, 2.200000000000001066 ) ) ;
#1753=CARTESIAN_POINT ( 'NONE',  ( 2.000000000000000000, -1.773042676681341856, 2.276824562219559311E-15 ) ) ;
#1757=CARTESIAN_POINT ( 'NONE',  ( 4.000000000000003553, 4.286263797015736595E-16, -3.500000000000000000 ) ) ;
#1768=DIRECTION ( 'NONE',  ( -1.000000000000000000, -0.000000000000000000, -0.000000000000000000 ) ) ;
#1770=DIRECTION ( 'NONE',  ( 0.000000000000000000, 0.000000000000000000, -1.000000000000000000 ) ) ;
#1780=( LENGTH_UNIT ( ) NAMED_UNIT ( * ) SI_UNIT ( .MILLI., .METRE. ) );
#1782=DIRECTION ( 'NONE',  ( 0.000000000000000000, 0.000000000000000000, 1.000000000000000000 ) ) ;
#1784=MECHANICAL_DESIGN_GEOMETRIC_PRESENTATION_REPRESENTATION('',(#2440),#1245);
#1789=CIRCLE ( 'NONE', #3323, 1.535500000000000087 ) ;
#1799=ORIENTED_EDGE ( 'NONE', *, *, #545, .F. ) ;
#1805=CARTESIAN_POINT ( 'NONE',  ( 2.000000000000000000, 1.329782007511004727, -0.7677500000000018199 ) ) ;
#1806=CARTESIAN_POINT ( 'NONE',  ( 2.000000000000000000, 1.773042676681340524, -2.059984127722458425E-15 ) ) ;
#1810=ORIENTED_EDGE ( 'NONE', *, *, #1661, .F. ) ;
#1816=CARTESIAN_POINT ( 'NONE',  ( 2.000000000000000000, -0.8865213383406694847, 1.535500000000001419 ) ) ;
#1831=ORIENTED_EDGE ( 'NONE', *, *, #886, .T. ) ;
#1834=CIRCLE ( 'NONE', #2271, 2.000000000000000888 ) ;
#1835=DIRECTION ( 'NONE',  ( 0.000000000000000000, -1.000000000000000000, 9.783878858594328898E-16 ) ) ;
#1847=AXIS2_PLACEMENT_3D ( 'NONE', #1516, #544, #2317 ) ;
#1860=ADVANCED_FACE ( 'NONE', ( #2504 ), #1735, .T. ) ;
#1863=ORIENTED_EDGE ( 'NONE', *, *, #2243, .T. ) ;
#1871=CARTESIAN_POINT ( 'NONE',  ( 0.000000000000000000, 0.000000000000000000, 0.000000000000000000 ) ) ;
#1872=CARTESIAN_POINT ( 'NONE',  ( 10.00000000000000178, 0.000000000000000000, 0.000000000000000000 ) ) ;
#1886=DIRECTION ( 'NONE',  ( 0.000000000000000000, 0.000000000000000000, 1.000000000000000000 ) ) ;
#1888=LINE ( 'NONE', #1415, #3220 ) ;
#1893=CYLINDRICAL_SURFACE ( 'NONE', #2934, 2.000000000000000888 ) ;
#1895=CIRCLE ( 'NONE', #2601, 3.500000000000000000 ) ;
#1899=CONICAL_SURFACE ( 'NONE', #428, 1.610000000000000098, 0.7853981633974652654 ) ;
#1904=CARTESIAN_POINT ( 'NONE',  ( 0.000000000000000000, -0.8865213383406694847, 1.535500000000001419 ) ) ;
#1908=EDGE_CURVE ( 'NONE', #595, #859, #1689, .T. ) ;
#1912=ORIENTED_EDGE ( 'NONE', *, *, #144, .T. ) ;
#1913=EDGE_CURVE ( 'NONE', #788, #887, #3265, .T. ) ;
#1926=VERTEX_POINT ( 'NONE', #1753 ) ;
#1941=PLANE ( 'NONE',  #2068 ) ;
#1951=DIRECTION ( 'NONE',  ( -1.000000000000000000, -0.000000000000000000, -0.000000000000000000 ) ) ;
#1952=VECTOR ( 'NONE', #2971, 1000.000000000000000 ) ;
#1955=DIRECTION ( 'NONE',  ( 0.000000000000000000, 0.000000000000000000, 1.000000000000000000 ) ) ;
#1958=CIRCLE ( 'NONE', #2888, 1.535500000000000087 ) ;
#1962=MECHANICAL_DESIGN_GEOMETRIC_PRESENTATION_REPRESENTATION('',(#438),#3116);
#1965=VERTEX_POINT ( 'NONE', #117 ) ;
#1966=CARTESIAN_POINT ( 'NONE',  ( 2.000000000000000000, -0.8865213383406694847, 1.535500000000001419 ) ) ;
#1979=VERTEX_POINT ( 'NONE', #2533 ) ;
#1985=DIRECTION ( 'NONE',  ( 0.000000000000000000, 0.000000000000000000, 1.000000000000000000 ) ) ;
#1989=DIRECTION ( 'NONE',  ( 0.000000000000000000, 0.000000000000000000, 1.000000000000000000 ) ) ;
#1990=PLANE ( 'NONE',  #976 ) ;
#1999=CARTESIAN_POINT ( 'NONE',  ( 2.000000000000000000, 0.8865213383406680414, -1.535500000000000975 ) ) ;
#2000=AXIS2_PLACEMENT_3D ( 'NONE', #3029, #1734, #3279 ) ;
#2004=PLANE ( 'NONE',  #3155 ) ;
#2007=AXIS2_PLACEMENT_3D ( 'NONE', #2593, #2343, #8 ) ;
#2010=AXIS2_PLACEMENT_3D ( 'NONE', #712, #1413, #1955 ) ;
#2015=EDGE_CURVE ( 'NONE', #1979, #2597, #1059, .T. ) ;
#2016=ORIENTED_EDGE ( 'NONE', *, *, #1913, .T. ) ;
#2026=VERTEX_POINT ( 'NONE', #3139 ) ;
#2036=CARTESIAN_POINT ( 'NONE',  ( 0.000000000000000000, 4.163799117101000559E-16, -3.299999999999999822 ) ) ;
#2043=ORIENTED_EDGE ( 'NONE', *, *, #1369, .T. ) ;
#2045=CARTESIAN_POINT ( 'NONE',  ( 2.000000000000000000, 1.880445160090761061E-16, -1.535500000000000087 ) ) ;
#2047=CARTESIAN_POINT ( 'NONE',  ( 2.000000000000000000, -1.329782007511007169, -0.7677499999999988223 ) ) ;
#2050=ORIENTED_EDGE ( 'NONE', *, *, #1276, .T. ) ;
#2052=PRODUCT_DEFINITION_CONTEXT ( 'detailed design', #396, 'design' ) ;
#2054=VERTEX_POINT ( 'NONE', #1003 ) ;
#2055=EDGE_CURVE ( 'NONE', #2072, #2365, #2081, .T. ) ;
#2060=VECTOR ( 'NONE', #3192, 1000.000000000000114 ) ;
#2062=DIRECTION ( 'NONE',  ( 0.000000000000000000, 0.000000000000000000, -1.000000000000000000 ) ) ;
#2064=VECTOR ( 'NONE', #1768, 1000.000000000000000 ) ;
#2066=VECTOR ( 'NONE', #668, 1000.000000000000114 ) ;
#2068=AXIS2_PLACEMENT_3D ( 'NONE', #2987, #73, #397 ) ;
#2069=CIRCLE ( 'NONE', #591, 2.200000000000001066 ) ;
#2070=ORIENTED_EDGE ( 'NONE', *, *, #2876, .T. ) ;
#2072=VERTEX_POINT ( 'NONE', #1631 ) ;
#2073=DIRECTION ( 'NONE',  ( -0.5000000000000061062, 0.000000000000000000, 0.8660254037844351549 ) ) ;
#2078=VERTEX_POINT ( 'NONE', #2684 ) ;
#2081=LINE ( 'NONE', #2045, #807 ) ;
#2085=ORIENTED_EDGE ( 'NONE', *, *, #1369, .F. ) ;
#2087=CARTESIAN_POINT ( 'NONE',  ( 2.000000000000000000, -0.8865213383406730374, -1.535499999999999421 ) ) ;
#2091=UNCERTAINTY_MEASURE_WITH_UNIT (LENGTH_MEASURE( 1.000000000000000082E-05 ), #3069, 'distance_accuracy_value', 'NONE');
#2093=DIRECTION ( 'NONE',  ( 0.000000000000000000, -0.4999999999999991118, 0.8660254037844391517 ) ) ;
#2097=EDGE_CURVE ( 'NONE', #2078, #2054, #45, .T. ) ;
#2100=VERTEX_POINT ( 'NONE', #604 ) ;
#2113=AXIS2_PLACEMENT_3D ( 'NONE', #2964, #3002, #621 ) ;
#2134=VECTOR ( 'NONE', #1477, 1000.000000000000000 ) ;
#2135=DIRECTION ( 'NONE',  ( 0.000000000000000000, 0.000000000000000000, -1.000000000000000000 ) ) ;
#2139=EDGE_LOOP ( 'NONE', ( #582, #2167, #2852, #1087 ) ) ;
#2141=FACE_OUTER_BOUND ( 'NONE', #2666, .T. ) ;
#2148=DIRECTION ( 'NONE',  ( 0.000000000000000000, 0.000000000000000000, -1.000000000000000000 ) ) ;
#2154=DIRECTION ( 'NONE',  ( -1.000000000000000000, -0.000000000000000000, -0.000000000000000000 ) ) ;
#2156=CARTESIAN_POINT ( 'NONE',  ( -31.74999999999995737, 0.000000000000000000, 0.000000000000000000 ) ) ;
#2157=ADVANCED_FACE ( 'NONE', ( #2895 ), #2822, .F. ) ;
#2162=CARTESIAN_POINT ( 'NONE',  ( 10.00000000000000178, 0.000000000000000000, 1.610000000000000098 ) ) ;
#2167=ORIENTED_EDGE ( 'NONE', *, *, #997, .T. ) ;
#2168=DIRECTION ( 'NONE',  ( 0.000000000000000000, 0.000000000000000000, -1.000000000000000000 ) ) ;
#2169=AXIS2_PLACEMENT_3D ( 'NONE', #1077, #319, #2148 ) ;
#2172=EDGE_CURVE ( 'NONE', #575, #2435, #79, .T. ) ;
#2177=AXIS2_PLACEMENT_3D ( 'NONE', #3138, #110, #2465 ) ;
#2179=CIRCLE ( 'NONE', #648, 2.000000000000000888 ) ;
#2181=ORIENTED_EDGE ( 'NONE', *, *, #416, .T. ) ;
#2189=ORIENTED_EDGE ( 'NONE', *, *, #3017, .T. ) ;
#2190=CARTESIAN_POINT ( 'NONE',  ( 2.000000000000000000, 2.065682573263594481E-15, 1.535500000000000309 ) ) ;
#2191=FACE_OUTER_BOUND ( 'NONE', #1498, .T. ) ;
#2197=LINE ( 'NONE', #2977, #2134 ) ;
#2217=ORIENTED_EDGE ( 'NONE', *, *, #1742, .T. ) ;
#2218=LINE ( 'NONE', #2541, #2877 ) ;
#2223=AXIS2_PLACEMENT_3D ( 'NONE', #1664, #2515, #2699 ) ;
#2225=PLANE ( 'NONE',  #2223 ) ;
#2228=PLANE ( 'NONE',  #2000 ) ;
#2243=EDGE_CURVE ( 'NONE', #2597, #880, #363, .T. ) ;
#2244=LINE ( 'NONE', #1665, #2494 ) ;
#2249=DIRECTION ( 'NONE',  ( 0.000000000000000000, 0.000000000000000000, -1.000000000000000000 ) ) ;
#2252=VERTEX_POINT ( 'NONE', #1212 ) ;
#2263=DIRECTION ( 'NONE',  ( 0.000000000000000000, -0.5000000000000011102, -0.8660254037844379305 ) ) ;
#2266=CIRCLE ( 'NONE', #1236, 3.299999999999999822 ) ;
#2267=DIRECTION ( 'NONE',  ( -1.000000000000000000, -0.000000000000000000, -0.000000000000000000 ) ) ;
#2271=AXIS2_PLACEMENT_3D ( 'NONE', #3085, #745, #730 ) ;
#2274=FACE_OUTER_BOUND ( 'NONE', #892, .T. ) ;
#2292=CARTESIAN_POINT ( 'NONE',  ( 0.000000000000000000, 0.8865213383406680414, -1.535500000000000975 ) ) ;
#2298=DIRECTION ( 'NONE',  ( -1.000000000000000000, -0.000000000000000000, -0.000000000000000000 ) ) ;
#2303=EDGE_CURVE ( 'NONE', #1203, #2435, #2197, .T. ) ;
#2304=DIRECTION ( 'NONE',  ( 1.000000000000000000, 0.000000000000000000, 0.000000000000000000 ) ) ;
#2307=CARTESIAN_POINT ( 'NONE',  ( 4.200000000000001954, 0.000000000000000000, 0.000000000000000000 ) ) ;
#2308=ADVANCED_FACE ( 'NONE', ( #2470 ), #2225, .F. ) ;
#2313=CARTESIAN_POINT ( 'NONE',  ( 2.000000000000000000, 1.773042676681340524, -2.059984127722458425E-15 ) ) ;
#2314=EDGE_CURVE ( 'NONE', #2435, #3240, #1428, .T. ) ;
#2317=DIRECTION ( 'NONE',  ( 0.000000000000000000, 0.000000000000000000, 1.000000000000000000 ) ) ;
#2318=DIRECTION ( 'NONE',  ( 0.000000000000000000, 0.000000000000000000, -1.000000000000000000 ) ) ;
#2319=ORIENTED_EDGE ( 'NONE', *, *, #205, .T. ) ;
#2322=AXIS2_PLACEMENT_3D ( 'NONE', #923, #2780, #2705 ) ;
#2328=AXIS2_PLACEMENT_3D ( 'NONE', #1146, #2927, #2135 ) ;
#2343=DIRECTION ( 'NONE',  ( 1.000000000000000000, 0.000000000000000000, 0.000000000000000000 ) ) ;
#2344=VECTOR ( 'NONE', #2263, 1000.000000000000114 ) ;
#2357=DIRECTION ( 'NONE',  ( 0.000000000000000000, -1.000000000000000000, 0.000000000000000000 ) ) ;
#2363=LINE ( 'NONE', #27, #157 ) ;
#2365=VERTEX_POINT ( 'NONE', #683 ) ;
#2373=ORIENTED_EDGE ( 'NONE', *, *, #90, .T. ) ;
#2376=ORIENTED_EDGE ( 'NONE', *, *, #1276, .F. ) ;
#2378=EDGE_CURVE ( 'NONE', #820, #2026, #640, .T. ) ;
#2382=DIRECTION ( 'NONE',  ( 0.000000000000000000, 0.000000000000000000, 1.000000000000000000 ) ) ;
#2388=ORIENTED_EDGE ( 'NONE', *, *, #1908, .T. ) ;
#2393=AXIS2_PLACEMENT_3D ( 'NONE', #889, #1672, #873 ) ;
#2401=PRODUCT_DEFINITION_FORMATION_WITH_SPECIFIED_SOURCE ( 'ANY', '', #2796, .NOT_KNOWN. ) ;
#2403=CARTESIAN_POINT ( 'NONE',  ( 2.000000000000000000, 1.773042676681340524, -2.059984127722458425E-15 ) ) ;
#2409=ORIENTED_EDGE ( 'NONE', *, *, #2055, .F. ) ;
#2412=ORIENTED_EDGE ( 'NONE', *, *, #1742, .F. ) ;
#2422=CARTESIAN_POINT ( 'NONE',  ( 4.000000000000003553, 0.000000000000000000, 3.500000000000000000 ) ) ;
#2424=ORIENTED_EDGE ( 'NONE', *, *, #2624, .T. ) ;
#2426=SURFACE_SIDE_STYLE ('',( #1071 ) ) ;
#2427=EDGE_LOOP ( 'NONE', ( #306, #1067, #155, #3369, #2886, #3011 ) ) ;
#2433=CIRCLE ( 'NONE', #2760, 1.535500000000000087 ) ;
#2435=VERTEX_POINT ( 'NONE', #2803 ) ;
#2440=STYLED_ITEM('',(#3422),#573);
#2442=AXIS2_PLACEMENT_3D ( 'NONE', #1143, #3178, #2948 ) ;
#2445=CARTESIAN_POINT ( 'NONE',  ( 4.200000000000001954, 0.000000000000000000, 2.000000000000000888 ) ) ;
#2465=DIRECTION ( 'NONE',  ( 0.000000000000000000, 0.000000000000000000, 1.000000000000000000 ) ) ;
#2470=FACE_OUTER_BOUND ( 'NONE', #1396, .T. ) ;
#2474=PLANE ( 'NONE',  #2322 ) ;
#2479=FACE_OUTER_BOUND ( 'NONE', #2139, .T. ) ;
#2487=CARTESIAN_POINT ( 'NONE',  ( 2.000000000000000000, 0.000000000000000000, 0.000000000000000000 ) ) ;
#2488=CARTESIAN_POINT ( 'NONE',  ( 2.000000000000000000, 1.773042676681340524, -2.059984127722458425E-15 ) ) ;
#2489=ADVANCED_FACE ( 'NONE', ( #2274 ), #779, .T. ) ;
#2494=VECTOR ( 'NONE', #1441, 1000.000000000000000 ) ;
#2499=CARTESIAN_POINT ( 'NONE',  ( 10.00000000000000178, 0.000000000000000000, 0.000000000000000000 ) ) ;
#2501=VECTOR ( 'NONE', #563, 1000.000000000000000 ) ;
#2504=FACE_OUTER_BOUND ( 'NONE', #3305, .T. ) ;
#2505=CARTESIAN_POINT ( 'NONE',  ( 0.000000000000000000, 0.000000000000000000, 0.000000000000000000 ) ) ;
#2509=ORIENTED_EDGE ( 'NONE', *, *, #708, .T. ) ;
#2511=ADVANCED_FACE ( 'NONE', ( #3306 ), #963, .F. ) ;
#2513=ORIENTED_EDGE ( 'NONE', *, *, #288, .T. ) ;
#2515=DIRECTION ( 'NONE',  ( 0.000000000000000000, 0.8660254037844380415, -0.5000000000000012212 ) ) ;
#2517=CYLINDRICAL_SURFACE ( 'NONE', #2113, 2.000000000000000888 ) ;
#2521=EDGE_CURVE ( 'NONE', #880, #940, #841, .T. ) ;
#2533=CARTESIAN_POINT ( 'NONE',  ( 2.000000000000000000, 1.773042676681340524, -2.059984127722458425E-15 ) ) ;
#2536=CARTESIAN_POINT ( 'NONE',  ( 2.000000000000000000, -1.773042676681341856, 2.276824562219559311E-15 ) ) ;
#2540=ORIENTED_EDGE ( 'NONE', *, *, #374, .T. ) ;
#2541=CARTESIAN_POINT ( 'NONE',  ( 2.000000000000000000, 0.8865213383406680414, -1.535500000000000975 ) ) ;
#2552=EDGE_CURVE ( 'NONE', #1926, #223, #2363, .T. ) ;
#2564=CARTESIAN_POINT ( 'NONE',  ( 2.000000000000000000, 0.000000000000000000, 1.535500000000000087 ) ) ;
#2565=UNCERTAINTY_MEASURE_WITH_UNIT (LENGTH_MEASURE( 1.000000000000000082E-05 ), #567, 'distance_accuracy_value', 'NONE');
#2588=DIRECTION ( 'NONE',  ( 0.000000000000000000, 0.000000000000000000, 1.000000000000000000 ) ) ;
#2590=DIRECTION ( 'NONE',  ( -1.000000000000000000, -0.000000000000000000, -0.000000000000000000 ) ) ;
#2592=ORIENTED_EDGE ( 'NONE', *, *, #159, .T. ) ;
#2593=CARTESIAN_POINT ( 'NONE',  ( 2.000000000000000000, 1.773042676681340524, -2.059984127722458425E-15 ) ) ;
#2597=VERTEX_POINT ( 'NONE', #566 ) ;
#2601=AXIS2_PLACEMENT_3D ( 'NONE', #3193, #571, #2382 ) ;
#2606=CARTESIAN_POINT ( 'NONE',  ( 4.200000000000001954, 0.000000000000000000, 0.000000000000000000 ) ) ;
#2607=AXIS2_PLACEMENT_3D ( 'NONE', #3316, #2267, #199 ) ;
#2611=PRODUCT_DEFINITION_SHAPE ( 'NONE', 'NONE',  #273 ) ;
#2619=ORIENTED_EDGE ( 'NONE', *, *, #2755, .T. ) ;
#2624=EDGE_CURVE ( 'NONE', #1054, #1203, #1673, .T. ) ;
#2626=FACE_OUTER_BOUND ( 'NONE', #905, .T. ) ;
#2629=CARTESIAN_POINT ( 'NONE',  ( 0.1999999999999987899, 0.000000000000000000, 3.299999999999999822 ) ) ;
#2630=ORIENTED_EDGE ( 'NONE', *, *, #2911, .F. ) ;
#2632=EDGE_LOOP ( 'NONE', ( #34, #1733, #281, #2694 ) ) ;
#2639=DIRECTION ( 'NONE',  ( 1.000000000000000000, 0.000000000000000000, 0.000000000000000000 ) ) ;
#2642=DIRECTION ( 'NONE',  ( -1.000000000000000000, -0.000000000000000000, -0.000000000000000000 ) ) ;
#2655=AXIS2_PLACEMENT_3D ( 'NONE', #1872, #2913, #1392 ) ;
#2666=EDGE_LOOP ( 'NONE', ( #3050, #1065, #1385, #2513 ) ) ;
#2669=FILL_AREA_STYLE ('',( #601 ) ) ;
#2671=ADVANCED_FACE ( 'NONE', ( #2191 ), #697, .F. ) ;
#2674=LINE ( 'NONE', #338, #1622 ) ;
#2676=ORIENTED_EDGE ( 'NONE', *, *, #2943, .T. ) ;
#2679=ADVANCED_FACE ( 'NONE', ( #904 ), #1941, .T. ) ;
#2684=CARTESIAN_POINT ( 'NONE',  ( 0.000000000000000000, -0.8865213383406694847, 1.535500000000001419 ) ) ;
#2693=DIRECTION ( 'NONE',  ( 1.000000000000000000, 0.000000000000000000, 0.000000000000000000 ) ) ;
#2694=ORIENTED_EDGE ( 'NONE', *, *, #3024, .F. ) ;
#2695=CARTESIAN_POINT ( 'NONE',  ( -31.74999999999995737, 4.286263797015736595E-16, -3.500000000000000000 ) ) ;
#2697=EDGE_LOOP ( 'NONE', ( #2961, #599, #3130, #2813, #2373 ) ) ;
#2698=ADVANCED_FACE ( 'NONE', ( #2141 ), #1893, .T. ) ;
#2699=DIRECTION ( 'NONE',  ( 0.000000000000000000, 0.5000000000000011102, 0.8660254037844379305 ) ) ;
#2703=LINE ( 'NONE', #607, #3047 ) ;
#2705=DIRECTION ( 'NONE',  ( -0.000000000000000000, 0.000000000000000000, 1.000000000000000000 ) ) ;
#2710=VECTOR ( 'NONE', #2093, 1000.000000000000000 ) ;
#2716=AXIS2_PLACEMENT_3D ( 'NONE', #2629, #2357, #2318 ) ;
#2735=DIRECTION ( 'NONE',  ( 0.000000000000000000, -0.5000000000000011102, -0.8660254037844379305 ) ) ;
#2748=ORIENTED_EDGE ( 'NONE', *, *, #2755, .F. ) ;
#2755=EDGE_CURVE ( 'NONE', #887, #21, #2768, .T. ) ;
#2760=AXIS2_PLACEMENT_3D ( 'NONE', #2487, #1466, #1231 ) ;
#2768=CIRCLE ( 'NONE', #2607, 2.200000000000001066 ) ;
#2780=DIRECTION ( 'NONE',  ( -1.000000000000000000, 0.000000000000000000, -0.000000000000000000 ) ) ;
#2782=ORIENTED_EDGE ( 'NONE', *, *, #898, .F. ) ;
#2783=LINE ( 'NONE', #1966, #2066 ) ;
#2795=DIRECTION ( 'NONE',  ( 0.000000000000000000, -1.000000000000000000, 1.345283343056720273E-15 ) ) ;
#2796=PRODUCT ( 'socket head cap screw_iso_ISO 4762 M4 x 6 - 6N', 'socket head cap screw_iso_ISO 4762 M4 x 6 - 6N', '', ( #401 ) ) ;
#2798=ORIENTED_EDGE ( 'NONE', *, *, #1134, .F. ) ;
#2803=CARTESIAN_POINT ( 'NONE',  ( 2.000000000000000000, 0.8865213383406715941, 1.535499999999999199 ) ) ;
#2813=ORIENTED_EDGE ( 'NONE', *, *, #658, .T. ) ;
#2815=VECTOR ( 'NONE', #522, 1000.000000000000114 ) ;
#2822=CONICAL_SURFACE ( 'NONE', #2442, 1.535500000000000087, 1.047197551196590748 ) ;
#2823=AXIS2_PLACEMENT_3D ( 'NONE', #2307, #776, #2835 ) ;
#2829=AXIS2_PLACEMENT_3D ( 'NONE', #773, #2304, #3112 ) ;
#2830=PLANE ( 'NONE',  #1294 ) ;
#2834=VERTEX_POINT ( 'NONE', #1537 ) ;
#2835=DIRECTION ( 'NONE',  ( 0.000000000000000000, 0.000000000000000000, -1.000000000000000000 ) ) ;
#2836=UNCERTAINTY_MEASURE_WITH_UNIT (LENGTH_MEASURE( 1.000000000000000082E-05 ), #1780, 'distance_accuracy_value', 'NONE');
#2840=EDGE_LOOP ( 'NONE', ( #297, #1491, #1081, #1094, #335 ) ) ;
#2845=( NAMED_UNIT ( * ) PLANE_ANGLE_UNIT ( ) SI_UNIT ( $, .RADIAN. ) );
#2852=ORIENTED_EDGE ( 'NONE', *, *, #159, .F. ) ;
#2853=EDGE_CURVE ( 'NONE', #2252, #595, #979, .T. ) ;
#2854=FACE_OUTER_BOUND ( 'NONE', #1671, .T. ) ;
#2857=ORIENTED_EDGE ( 'NONE', *, *, #2314, .F. ) ;
#2860=DIRECTION ( 'NONE',  ( 1.000000000000000000, 0.000000000000000000, 0.000000000000000000 ) ) ;
#2861=FACE_OUTER_BOUND ( 'NONE', #3361, .T. ) ;
#2867=DIRECTION ( 'NONE',  ( 0.000000000000000000, 0.000000000000000000, 1.000000000000000000 ) ) ;
#2876=EDGE_CURVE ( 'NONE', #2078, #3240, #819, .T. ) ;
#2877=VECTOR ( 'NONE', #3076, 1000.000000000000000 ) ;
#2880=LINE ( 'NONE', #274, #269 ) ;
#2883=DIRECTION ( 'NONE',  ( 0.000000000000000000, 1.000000000000000000, -1.345283343056720273E-15 ) ) ;
#2886=ORIENTED_EDGE ( 'NONE', *, *, #2521, .F. ) ;
#2887=CARTESIAN_POINT ( 'NONE',  ( 2.000000000000000000, 1.773042676681340524, -2.059984127722458425E-15 ) ) ;
#2888=AXIS2_PLACEMENT_3D ( 'NONE', #3140, #1075, #1019 ) ;
#2892=DIRECTION ( 'NONE',  ( 0.000000000000000000, 0.4999999999999989453, -0.8660254037844391517 ) ) ;
#2895=FACE_OUTER_BOUND ( 'NONE', #2697, .T. ) ;
#2899=CARTESIAN_POINT ( 'NONE',  ( 4.000000000000003553, 0.000000000000000000, 0.000000000000000000 ) ) ;
#2911=EDGE_CURVE ( 'NONE', #1274, #1395, #1305, .T. ) ;
#2913=DIRECTION ( 'NONE',  ( -1.000000000000000000, -0.000000000000000000, -0.000000000000000000 ) ) ;
#2922=DIRECTION ( 'NONE',  ( 0.000000000000000000, 0.000000000000000000, 1.000000000000000000 ) ) ;
#2925=ORIENTED_EDGE ( 'NONE', *, *, #295, .T. ) ;
#2927=DIRECTION ( 'NONE',  ( 1.000000000000000000, 0.000000000000000000, 0.000000000000000000 ) ) ;
#2934=AXIS2_PLACEMENT_3D ( 'NONE', #1399, #2154, #3187 ) ;
#2935=VECTOR ( 'NONE', #1675, 1000.000000000000000 ) ;
#2938=CIRCLE ( 'NONE', #2829, 3.500000000000000000 ) ;
#2943=EDGE_CURVE ( 'NONE', #436, #2252, #2938, .T. ) ;
#2948=DIRECTION ( 'NONE',  ( 0.000000000000000000, 0.000000000000000000, 1.000000000000000000 ) ) ;
#2961=ORIENTED_EDGE ( 'NONE', *, *, #1080, .F. ) ;
#2964=CARTESIAN_POINT ( 'NONE',  ( -31.74999999999995737, 0.000000000000000000, 0.000000000000000000 ) ) ;
#2965=DIRECTION ( 'NONE',  ( 0.000000000000000000, -0.4999999999999991118, 0.8660254037844391517 ) ) ;
#2968=VERTEX_POINT ( 'NONE', #3183 ) ;
#2971=DIRECTION ( 'NONE',  ( 0.000000000000000000, 1.000000000000000000, -1.345283343056720273E-15 ) ) ;
#2977=CARTESIAN_POINT ( 'NONE',  ( 2.000000000000000000, -0.8865213383406694847, 1.535500000000001419 ) ) ;
#2981=CIRCLE ( 'NONE', #474, 1.535500000000000087 ) ;
#2985=FACE_OUTER_BOUND ( 'NONE', #2840, .T. ) ;
#2987=CARTESIAN_POINT ( 'NONE',  ( 2.000000000000000000, 1.773042676681340524, -2.059984127722458425E-15 ) ) ;
#3001=COLOUR_RGB ( '',1.000000000000000000, 0.9490196078431372140, 0.9098039215686274384 ) ;
#3002=DIRECTION ( 'NONE',  ( -1.000000000000000000, -0.000000000000000000, -0.000000000000000000 ) ) ;
#3003=CARTESIAN_POINT ( 'NONE',  ( 4.200000000000001954, 2.694222958124178486E-16, 2.200000000000001066 ) ) ;
#3011=ORIENTED_EDGE ( 'NONE', *, *, #2243, .F. ) ;
#3013=EDGE_CURVE ( 'NONE', #1395, #1274, #378, .T. ) ;
#3015=FACE_BOUND ( 'NONE', #258, .T. ) ;
#3017=EDGE_CURVE ( 'NONE', #1926, #2054, #2703, .T. ) ;
#3019=CARTESIAN_POINT ( 'NONE',  ( 9.610000000000013642, 0.000000000000000000, 2.000000000000000888 ) ) ;
#3022=ORIENTED_EDGE ( 'NONE', *, *, #220, .F. ) ;
#3024=EDGE_CURVE ( 'NONE', #1965, #28, #2179, .T. ) ;
#3027=CARTESIAN_POINT ( 'NONE',  ( 2.000000000000000000, 0.8865213383406715941, 1.535499999999999199 ) ) ;
#3028=EDGE_LOOP ( 'NONE', ( #2070, #2857, #908, #512, #2043 ) ) ;
#3029=CARTESIAN_POINT ( 'NONE',  ( 4.000000000000000000, 3.500000000000000000, 0.000000000000000000 ) ) ;
#3032=DIRECTION ( 'NONE',  ( -1.000000000000000000, -0.000000000000000000, -0.000000000000000000 ) ) ;
#3033=EDGE_CURVE ( 'NONE', #1965, #2968, #1888, .T. ) ;
#3047=VECTOR ( 'NONE', #371, 1000.000000000000000 ) ;
#3050=ORIENTED_EDGE ( 'NONE', *, *, #3033, .F. ) ;
#3069=( LENGTH_UNIT ( ) NAMED_UNIT ( * ) SI_UNIT ( .MILLI., .METRE. ) );
#3071=CARTESIAN_POINT ( 'NONE',  ( 2.000000000000000000, 1.773042676681340524, -2.059984127722458425E-15 ) ) ;
#3074=EDGE_LOOP ( 'NONE', ( #2388, #3235 ) ) ;
#3075=ORIENTED_EDGE ( 'NONE', *, *, #708, .F. ) ;
#3076=DIRECTION ( 'NONE',  ( 0.000000000000000000, -1.000000000000000000, 9.783878858594328898E-16 ) ) ;
#3083=DIRECTION ( 'NONE',  ( -0.5000000000000061062, 1.060575238724902601E-16, -0.8660254037844351549 ) ) ;
#3085=CARTESIAN_POINT ( 'NONE',  ( 9.610000000000013642, 0.000000000000000000, 0.000000000000000000 ) ) ;
#3089=ORIENTED_EDGE ( 'NONE', *, *, #2853, .T. ) ;
#3102=EDGE_LOOP ( 'NONE', ( #2409, #947, #2925, #2319, #2509 ) ) ;
#3111=AXIS2_PLACEMENT_3D ( 'NONE', #1871, #3207, #2639 ) ;
#3112=DIRECTION ( 'NONE',  ( 0.000000000000000000, 0.000000000000000000, 1.000000000000000000 ) ) ;
#3115=DIRECTION ( 'NONE',  ( -0.7071067811865355823, 8.659560562355079537E-17, -0.7071067811865595631 ) ) ;
#3116=( GEOMETRIC_REPRESENTATION_CONTEXT ( 3 ) GLOBAL_UNCERTAINTY_ASSIGNED_CONTEXT ( ( #2565 ) ) GLOBAL_UNIT_ASSIGNED_CONTEXT ( ( #567, #1388, #1091 ) ) REPRESENTATION_CONTEXT ( 'NONE', 'WORKASPACE' ) );
#3128=FACE_OUTER_BOUND ( 'NONE', #64, .T. ) ;
#3130=ORIENTED_EDGE ( 'NONE', *, *, #3273, .T. ) ;
#3138=CARTESIAN_POINT ( 'NONE',  ( 2.000000000000000000, 0.000000000000000000, 0.000000000000000000 ) ) ;
#3139=CARTESIAN_POINT ( 'NONE',  ( 10.00000000000000178, 2.210487472460973191E-16, -1.610000000000000098 ) ) ;
#3140=CARTESIAN_POINT ( 'NONE',  ( 2.000000000000000000, 0.000000000000000000, 0.000000000000000000 ) ) ;
#3143=CARTESIAN_POINT ( 'NONE',  ( 0.000000000000000000, -0.8865213383406694847, 1.535500000000001419 ) ) ;
#3148=CLOSED_SHELL ( 'NONE', ( #2157, #1040, #2671, #918, #528, #846, #5, #570, #556, #2698, #389, #1860, #1107, #1473, #2679, #1358, #2489, #1346, #2511, #2308, #1422, #1127, #588, #1638, #3276, #187, #804 ) ) ;
#3149=ADVANCED_BREP_SHAPE_REPRESENTATION ( '', ( #573, #3111 ), #1101 ) ;
#3150=EDGE_LOOP ( 'NONE', ( #57, #2424, #440 ) ) ;
#3155=AXIS2_PLACEMENT_3D ( 'NONE', #2313, #1546, #1042 ) ;
#3158=AXIS2_PLACEMENT_3D ( 'NONE', #1593, #527, #2867 ) ;
#3160=DIRECTION ( 'NONE',  ( -1.000000000000000000, -0.000000000000000000, -0.000000000000000000 ) ) ;
#3168=EDGE_LOOP ( 'NONE', ( #844, #1366, #1655, #2181 ) ) ;
#3178=DIRECTION ( 'NONE',  ( -1.000000000000000000, -0.000000000000000000, -0.000000000000000000 ) ) ;
#3181=DIRECTION ( 'NONE',  ( 1.000000000000000000, 0.000000000000000000, 0.000000000000000000 ) ) ;
#3183=CARTESIAN_POINT ( 'NONE',  ( 4.200000000000001954, 2.449293598294707893E-16, -2.000000000000000888 ) ) ;
#3184=ORIENTED_EDGE ( 'NONE', *, *, #343, .F. ) ;
#3187=DIRECTION ( 'NONE',  ( 0.000000000000000000, 0.000000000000000000, 1.000000000000000000 ) ) ;
#3192=DIRECTION ( 'NONE',  ( 0.000000000000000000, -0.5000000000000011102, -0.8660254037844379305 ) ) ;
#3193=CARTESIAN_POINT ( 'NONE',  ( 0.1999999999999987899, 0.000000000000000000, 0.000000000000000000 ) ) ;
#3202=CARTESIAN_POINT ( 'NONE',  ( 10.00000000000000178, 0.000000000000000000, 1.610000000000000098 ) ) ;
#3205=CIRCLE ( 'NONE', #1512, 1.535500000000000087 ) ;
#3207=DIRECTION ( 'NONE',  ( 0.000000000000000000, 0.000000000000000000, 1.000000000000000000 ) ) ;
#3212=VECTOR ( 'NONE', #1835, 1000.000000000000000 ) ;
#3217=TOROIDAL_SURFACE ( 'NONE', #2823, 2.200000000000001066, 0.2000000000000000111 ) ;
#3218=ORIENTED_EDGE ( 'NONE', *, *, #1644, .F. ) ;
#3220=VECTOR ( 'NONE', #3234, 1000.000000000000000 ) ;
#3225=DIRECTION ( 'NONE',  ( -1.000000000000000000, -0.000000000000000000, -0.000000000000000000 ) ) ;
#3226=EDGE_CURVE ( 'NONE', #1054, #872, #184, .T. ) ;
#3232=LINE ( 'NONE', #899, #1568 ) ;
#3234=DIRECTION ( 'NONE',  ( -1.000000000000000000, -0.000000000000000000, -0.000000000000000000 ) ) ;
#3235=ORIENTED_EDGE ( 'NONE', *, *, #36, .T. ) ;
#3239=CARTESIAN_POINT ( 'NONE',  ( 4.200000000000001954, 0.000000000000000000, 0.000000000000000000 ) ) ;
#3240=VERTEX_POINT ( 'NONE', #249 ) ;
#3262=CIRCLE ( 'NONE', #2328, 2.000000000000000888 ) ;
#3265=CIRCLE ( 'NONE', #104, 0.2000000000000000944 ) ;
#3273=EDGE_CURVE ( 'NONE', #2365, #223, #1958, .T. ) ;
#3275=ORIENTED_EDGE ( 'NONE', *, *, #2015, .T. ) ;
#3276=ADVANCED_FACE ( 'NONE', ( #2626 ), #1548, .F. ) ;
#3279=DIRECTION ( 'NONE',  ( 0.000000000000000000, 0.000000000000000000, -1.000000000000000000 ) ) ;
#3293=ORIENTED_EDGE ( 'NONE', *, *, #2314, .T. ) ;
#3294=DIRECTION ( 'NONE',  ( -1.000000000000000000, -0.000000000000000000, -0.000000000000000000 ) ) ;
#3302=EDGE_LOOP ( 'NONE', ( #1303, #354, #1423 ) ) ;
#3305=EDGE_LOOP ( 'NONE', ( #1176, #1608 ) ) ;
#3306=FACE_OUTER_BOUND ( 'NONE', #964, .T. ) ;
#3316=CARTESIAN_POINT ( 'NONE',  ( 4.000000000000000000, 0.000000000000000000, 0.000000000000000000 ) ) ;
#3320=DIRECTION ( 'NONE',  ( 0.000000000000000000, 0.000000000000000000, 1.000000000000000000 ) ) ;
#3323=AXIS2_PLACEMENT_3D ( 'NONE', #383, #346, #2922 ) ;
#3328=DIRECTION ( 'NONE',  ( 0.000000000000000000, -9.783878858594328898E-16, -1.000000000000000000 ) ) ;
#3353=VERTEX_POINT ( 'NONE', #1805 ) ;
#3361=EDGE_LOOP ( 'NONE', ( #1035, #576, #3075 ) ) ;
#3365=CARTESIAN_POINT ( 'NONE',  ( 2.000000000000000000, 0.000000000000000000, 0.000000000000000000 ) ) ;
#3369=ORIENTED_EDGE ( 'NONE', *, *, #467, .T. ) ;
#3370=ORIENTED_EDGE ( 'NONE', *, *, #3273, .F. ) ;
#3416=COLOUR_RGB('Black',0.12,0.14,0.17);
#3417=FILL_AREA_STYLE_COLOUR('',#3416);
#3418=FILL_AREA_STYLE('',(#3417));
#3419=SURFACE_STYLE_FILL_AREA(#3418);
#3420=SURFACE_SIDE_STYLE('',(#3419));
#3421=SURFACE_STYLE_USAGE(.BOTH.,#3420);
#3422=PRESENTATION_STYLE_ASSIGNMENT((#3421));
ENDSEC;
END-ISO-10303-21;
